ISO-10303-21;
HEADER;
/* Generated by software containing ST-Developer
 * from STEP Tools, Inc. (www.steptools.com) 
 */

FILE_DESCRIPTION(
/* description */ ('Double-row support with tensioned shaft'),
/* implementation_level */ '2;1');

FILE_NAME(
/* name */ 'Flange hole reducer (7).step',
/* time_stamp */ '2026-10-27T10:50:35-07:00',
/* author */ (''),
/* organization */ (''),
/* preprocessor_version */ 'ST-DEVELOPER v20.2',
/* originating_system */ 'Autodesk Translation Framework v15.17.0.0',
/* authorisation */ '');

FILE_SCHEMA (('AUTOMOTIVE_DESIGN { 1 0 10303 214 3 1 1 }'));
ENDSEC;

DATA;
#10=MECHANICAL_DESIGN_GEOMETRIC_PRESENTATION_REPRESENTATION('',(#493),#11559);
#429=SHAPE_REPRESENTATION_RELATIONSHIP('SRR','None',#11737,#461);
#461=ADVANCED_BREP_SHAPE_REPRESENTATION('',(#526),#11539);
#493=STYLED_ITEM('',(#11981),#526);
#526=MANIFOLD_SOLID_BREP('Body1',#6338);
#608=FACE_BOUND('',#1430,.T.);
#609=FACE_BOUND('',#1432,.T.);
#739=PLANE('',#6916);
#740=PLANE('',#6917);
#1017=FACE_OUTER_BOUND('',#1427,.T.);
#1018=FACE_OUTER_BOUND('',#1428,.T.);
#1019=FACE_OUTER_BOUND('',#1429,.T.);
#1020=FACE_OUTER_BOUND('',#1431,.T.);
#1427=EDGE_LOOP('',(#4762,#4763,#4764,#4765));
#1428=EDGE_LOOP('',(#4766,#4767,#4768,#4769));
#1429=EDGE_LOOP('',(#4770));
#1430=EDGE_LOOP('',(#4771));
#1431=EDGE_LOOP('',(#4772));
#1432=EDGE_LOOP('',(#4773));
#1878=LINE('',#9715,#2425);
#1879=LINE('',#9721,#2426);
#2425=VECTOR('',#7905,0.425);
#2426=VECTOR('',#7912,0.595);
#2916=CIRCLE('',#6911,0.425);
#2917=CIRCLE('',#6912,0.425);
#2918=CIRCLE('',#6914,0.595);
#2919=CIRCLE('',#6915,0.595);
#3171=VERTEX_POINT('',#9712);
#3172=VERTEX_POINT('',#9714);
#3173=VERTEX_POINT('',#9718);
#3174=VERTEX_POINT('',#9720);
#3766=EDGE_CURVE('',#3171,#3171,#2916,.T.);
#3767=EDGE_CURVE('',#3171,#3172,#1878,.T.);
#3768=EDGE_CURVE('',#3172,#3172,#2917,.T.);
#3769=EDGE_CURVE('',#3173,#3173,#2918,.T.);
#3770=EDGE_CURVE('',#3173,#3174,#1879,.T.);
#3771=EDGE_CURVE('',#3174,#3174,#2919,.T.);
#4762=ORIENTED_EDGE('',*,*,#3766,.F.);
#4763=ORIENTED_EDGE('',*,*,#3767,.T.);
#4764=ORIENTED_EDGE('',*,*,#3768,.T.);
#4765=ORIENTED_EDGE('',*,*,#3767,.F.);
#4766=ORIENTED_EDGE('',*,*,#3769,.F.);
#4767=ORIENTED_EDGE('',*,*,#3770,.T.);
#4768=ORIENTED_EDGE('',*,*,#3771,.T.);
#4769=ORIENTED_EDGE('',*,*,#3770,.F.);
#4770=ORIENTED_EDGE('',*,*,#3769,.T.);
#4771=ORIENTED_EDGE('',*,*,#3766,.T.);
#4772=ORIENTED_EDGE('',*,*,#3771,.F.);
#4773=ORIENTED_EDGE('',*,*,#3768,.F.);
#5930=CYLINDRICAL_SURFACE('',#6910,0.425);
#5931=CYLINDRICAL_SURFACE('',#6913,0.595);
#6080=ADVANCED_FACE('',(#1017),#5930,.F.);
#6081=ADVANCED_FACE('',(#1018),#5931,.T.);
#6082=ADVANCED_FACE('',(#1019,#608),#739,.T.);
#6083=ADVANCED_FACE('',(#1020,#609),#740,.F.);
#6338=CLOSED_SHELL('',(#6080,#6081,#6082,#6083));
#6909=AXIS2_PLACEMENT_3D('',#9710,#7899,#7900);
#6910=AXIS2_PLACEMENT_3D('',#9711,#7901,#7902);
#6911=AXIS2_PLACEMENT_3D('',#9713,#7903,#7904);
#6912=AXIS2_PLACEMENT_3D('',#9716,#7906,#7907);
#6913=AXIS2_PLACEMENT_3D('',#9717,#7908,#7909);
#6914=AXIS2_PLACEMENT_3D('',#9719,#7910,#7911);
#6915=AXIS2_PLACEMENT_3D('',#9722,#7913,#7914);
#6916=AXIS2_PLACEMENT_3D('',#9723,#7915,#7916);
#6917=AXIS2_PLACEMENT_3D('',#9724,#7917,#7918);
#7899=DIRECTION('axis',(0.,0.,1.));
#7900=DIRECTION('refdir',(1.,0.,0.));
#7901=DIRECTION('center_axis',(0.,1.,0.));
#7902=DIRECTION('ref_axis',(1.,0.,0.));
#7903=DIRECTION('center_axis',(0.,-1.,0.));
#7904=DIRECTION('ref_axis',(1.,0.,0.));
#7905=DIRECTION('',(0.,-1.,0.));
#7906=DIRECTION('center_axis',(0.,-1.,0.));
#7907=DIRECTION('ref_axis',(1.,0.,0.));
#7908=DIRECTION('center_axis',(0.,1.,0.));
#7909=DIRECTION('ref_axis',(1.,0.,0.));
#7910=DIRECTION('center_axis',(0.,1.,0.));
#7911=DIRECTION('ref_axis',(1.,0.,0.));
#7912=DIRECTION('',(0.,-1.,0.));
#7913=DIRECTION('center_axis',(0.,1.,0.));
#7914=DIRECTION('ref_axis',(1.,0.,0.));
#7915=DIRECTION('center_axis',(0.,1.,0.));
#7916=DIRECTION('ref_axis',(1.,0.,0.));
#7917=DIRECTION('center_axis',(0.,1.,0.));
#7918=DIRECTION('ref_axis',(1.,0.,0.));
#9710=CARTESIAN_POINT('',(0.,0.,0.));
#9711=CARTESIAN_POINT('Origin',(3.2,17.5,13.2));
#9712=CARTESIAN_POINT('',(2.775,18.5,13.2));
#9713=CARTESIAN_POINT('Origin',(3.2,18.5,13.2));
#9714=CARTESIAN_POINT('',(2.775,17.5,13.2));
#9715=CARTESIAN_POINT('',(2.775,17.5,13.2));
#9716=CARTESIAN_POINT('Origin',(3.2,17.5,13.2));
#9717=CARTESIAN_POINT('Origin',(3.2,17.5,13.2));
#9718=CARTESIAN_POINT('',(2.605,18.5,13.2));
#9719=CARTESIAN_POINT('Origin',(3.2,18.5,13.2));
#9720=CARTESIAN_POINT('',(2.605,17.5,13.2));
#9721=CARTESIAN_POINT('',(2.605,17.5,13.2));
#9722=CARTESIAN_POINT('Origin',(3.2,17.5,13.2));
#9723=CARTESIAN_POINT('Origin',(3.2,18.5,13.2));
#9724=CARTESIAN_POINT('Origin',(3.2,17.5,13.2));
#11502=UNCERTAINTY_MEASURE_WITH_UNIT(LENGTH_MEASURE(0.001),#11560,
'DISTANCE_ACCURACY_VALUE',
'Maximum model space distance between geometric entities at asserted c
onnectivities');
#11522=UNCERTAINTY_MEASURE_WITH_UNIT(LENGTH_MEASURE(0.001),#11560,
'DISTANCE_ACCURACY_VALUE',
'Maximum model space distance between geometric entities at asserted c
onnectivities');
#11539=(
GEOMETRIC_REPRESENTATION_CONTEXT(3)
GLOBAL_UNCERTAINTY_ASSIGNED_CONTEXT((#11502))
GLOBAL_UNIT_ASSIGNED_CONTEXT((#11560,#11562,#11563))
REPRESENTATION_CONTEXT('','3D')
);
#11559=(
GEOMETRIC_REPRESENTATION_CONTEXT(3)
GLOBAL_UNCERTAINTY_ASSIGNED_CONTEXT((#11522))
GLOBAL_UNIT_ASSIGNED_CONTEXT((#11560,#11562,#11563))
REPRESENTATION_CONTEXT('','3D')
);
#11560=(
LENGTH_UNIT()
NAMED_UNIT(*)
SI_UNIT(.CENTI.,.METRE.)
);
#11562=(
NAMED_UNIT(*)
PLANE_ANGLE_UNIT()
SI_UNIT($,.RADIAN.)
);
#11563=(
NAMED_UNIT(*)
SI_UNIT($,.STERADIAN.)
SOLID_ANGLE_UNIT()
);
#11580=SHAPE_DEFINITION_REPRESENTATION(#11616,#11737);
#11616=PRODUCT_DEFINITION_SHAPE('',$,#11774);
#11737=SHAPE_REPRESENTATION('',(#6909),#11539);
#11757=PRODUCT_DEFINITION_CONTEXT('part definition',#11867,'design');
#11774=PRODUCT_DEFINITION('Flange hole reducer (7)',
'Flange hole reducer (7)',#11810,#11757);
#11810=PRODUCT_DEFINITION_FORMATION('',$,#11885);
#11867=APPLICATION_CONTEXT(
'Core Data for Automotive Mechanical Design Process');
#11868=PRODUCT_CONTEXT('part definition',#11867,'mechanical');
#11885=PRODUCT('Flange hole reducer (7)','Flange hole reducer (7)',
'Flange hole reducer (7)',(#11868));
#11975=COLOUR_RGB('Off White',0.89,0.88,0.83);
#11976=FILL_AREA_STYLE_COLOUR('',#11975);
#11977=FILL_AREA_STYLE('',(#11976));
#11978=SURFACE_STYLE_FILL_AREA(#11977);
#11979=SURFACE_SIDE_STYLE('',(#11978));
#11980=SURFACE_STYLE_USAGE(.BOTH.,#11979);
#11981=PRESENTATION_STYLE_ASSIGNMENT((#11980));
ENDSEC;
END-ISO-10303-21;
